ISO-10303-21;
HEADER;
/* Generated by software containing ST-Developer
 * from STEP Tools, Inc. (www.steptools.com) 
 */

FILE_DESCRIPTION(
/* description */ ('Chute with adjustable gate'),
/* implementation_level */ '2;1');

FILE_NAME(
/* name */ 'M5x14 Cap Screw.step',
/* time_stamp */ '2026-10-27T10:52:28-07:00',
/* author */ (''),
/* organization */ (''),
/* preprocessor_version */ 'ST-DEVELOPER v20.2',
/* originating_system */ 'Autodesk Translation Framework v15.17.0.0',
/* authorisation */ '');

FILE_SCHEMA (('AUTOMOTIVE_DESIGN { 1 0 10303 214 3 1 1 }'));
ENDSEC;

DATA;
#10=MECHANICAL_DESIGN_GEOMETRIC_PRESENTATION_REPRESENTATION('',(#444),#13094);
#329=ORIENTED_CLOSED_SHELL('',*,#7629,.F.);
#339=CONICAL_SURFACE('',#8586,0.4,0.785398163397448);
#340=CONICAL_SURFACE('',#8590,0.41,0.785398163397448);
#341=CONICAL_SURFACE('',#8594,0.26,0.463647609000806);
#348=BREP_WITH_VOIDS('Body1',#7630,(#329));
#380=SHAPE_REPRESENTATION_RELATIONSHIP('SRR','None',#13283,#412);
#412=ADVANCED_BREP_SHAPE_REPRESENTATION('',(#348),#13092);
#444=STYLED_ITEM('',(#13502),#348);
#588=FACE_BOUND('',#1839,.T.);
#892=PLANE('',#8574);
#893=PLANE('',#8575);
#894=PLANE('',#8576);
#895=PLANE('',#8577);
#896=PLANE('',#8578);
#897=PLANE('',#8579);
#898=PLANE('',#8580);
#899=PLANE('',#8581);
#900=PLANE('',#8582);
#901=PLANE('',#8584);
#902=PLANE('',#8592);
#1296=FACE_OUTER_BOUND('',#1825,.T.);
#1297=FACE_OUTER_BOUND('',#1826,.T.);
#1298=FACE_OUTER_BOUND('',#1827,.T.);
#1299=FACE_OUTER_BOUND('',#1828,.T.);
#1300=FACE_OUTER_BOUND('',#1829,.T.);
#1301=FACE_OUTER_BOUND('',#1830,.T.);
#1302=FACE_OUTER_BOUND('',#1831,.T.);
#1303=FACE_OUTER_BOUND('',#1832,.T.);
#1304=FACE_OUTER_BOUND('',#1833,.T.);
#1305=FACE_OUTER_BOUND('',#1834,.T.);
#1306=FACE_OUTER_BOUND('',#1835,.T.);
#1307=FACE_OUTER_BOUND('',#1836,.T.);
#1308=FACE_OUTER_BOUND('',#1837,.T.);
#1309=FACE_OUTER_BOUND('',#1838,.T.);
#1310=FACE_OUTER_BOUND('',#1840,.T.);
#1311=FACE_OUTER_BOUND('',#1841,.T.);
#1825=EDGE_LOOP('',(#6982,#6983,#6984,#6985));
#1826=EDGE_LOOP('',(#6986,#6987,#6988,#6989));
#1827=EDGE_LOOP('',(#6990,#6991,#6992,#6993));
#1828=EDGE_LOOP('',(#6994,#6995,#6996,#6997));
#1829=EDGE_LOOP('',(#6998,#6999,#7000,#7001));
#1830=EDGE_LOOP('',(#7002,#7003,#7004,#7005));
#1831=EDGE_LOOP('',(#7006,#7007,#7008,#7009,#7010,#7011));
#1832=EDGE_LOOP('',(#7012,#7013,#7014,#7015,#7016,#7017));
#1833=EDGE_LOOP('',(#7018));
#1834=EDGE_LOOP('',(#7019));
#1835=EDGE_LOOP('',(#7020,#7021,#7022,#7023));
#1836=EDGE_LOOP('',(#7024,#7025,#7026,#7027));
#1837=EDGE_LOOP('',(#7028,#7029,#7030,#7031));
#1838=EDGE_LOOP('',(#7032));
#1839=EDGE_LOOP('',(#7033));
#1840=EDGE_LOOP('',(#7034,#7035,#7036,#7037));
#1841=EDGE_LOOP('',(#7038,#7039,#7040,#7041));
#2590=LINE('',#12814,#3367);
#2591=LINE('',#12816,#3368);
#2592=LINE('',#12818,#3369);
#2593=LINE('',#12819,#3370);
#2594=LINE('',#12822,#3371);
#2595=LINE('',#12824,#3372);
#2596=LINE('',#12825,#3373);
#2597=LINE('',#12828,#3374);
#2598=LINE('',#12830,#3375);
#2599=LINE('',#12831,#3376);
#2600=LINE('',#12834,#3377);
#2601=LINE('',#12836,#3378);
#2602=LINE('',#12837,#3379);
#2603=LINE('',#12840,#3380);
#2604=LINE('',#12842,#3381);
#2605=LINE('',#12843,#3382);
#2606=LINE('',#12845,#3383);
#2607=LINE('',#12846,#3384);
#2608=LINE('',#12858,#3385);
#2609=LINE('',#12862,#3386);
#2610=LINE('',#12866,#3387);
#2611=LINE('',#12873,#3388);
#2612=LINE('',#12875,#3389);
#3367=VECTOR('',#10606,1.);
#3368=VECTOR('',#10607,1.);
#3369=VECTOR('',#10608,1.);
#3370=VECTOR('',#10609,1.);
#3371=VECTOR('',#10612,1.);
#3372=VECTOR('',#10613,1.);
#3373=VECTOR('',#10614,1.);
#3374=VECTOR('',#10617,1.);
#3375=VECTOR('',#10618,1.);
#3376=VECTOR('',#10619,1.);
#3377=VECTOR('',#10622,1.);
#3378=VECTOR('',#10623,1.);
#3379=VECTOR('',#10624,1.);
#3380=VECTOR('',#10627,1.);
#3381=VECTOR('',#10628,1.);
#3382=VECTOR('',#10629,1.);
#3383=VECTOR('',#10632,1.);
#3384=VECTOR('',#10633,1.);
#3385=VECTOR('',#10650,0.4);
#3386=VECTOR('',#10655,0.425);
#3387=VECTOR('',#10660,0.41);
#3388=VECTOR('',#10669,0.26);
#3389=VECTOR('',#10672,0.25);
#3578=CIRCLE('',#8583,0.24505);
#3579=CIRCLE('',#8585,0.375);
#3580=CIRCLE('',#8587,0.425);
#3581=CIRCLE('',#8589,0.425);
#3582=CIRCLE('',#8591,0.395);
#3583=CIRCLE('',#8593,0.27);
#3584=CIRCLE('',#8595,0.24505);
#4187=VERTEX_POINT('',#12812);
#4188=VERTEX_POINT('',#12813);
#4189=VERTEX_POINT('',#12815);
#4190=VERTEX_POINT('',#12817);
#4191=VERTEX_POINT('',#12821);
#4192=VERTEX_POINT('',#12823);
#4193=VERTEX_POINT('',#12827);
#4194=VERTEX_POINT('',#12829);
#4195=VERTEX_POINT('',#12833);
#4196=VERTEX_POINT('',#12835);
#4197=VERTEX_POINT('',#12839);
#4198=VERTEX_POINT('',#12841);
#4199=VERTEX_POINT('',#12850);
#4200=VERTEX_POINT('',#12853);
#4201=VERTEX_POINT('',#12856);
#4202=VERTEX_POINT('',#12860);
#4203=VERTEX_POINT('',#12864);
#4204=VERTEX_POINT('',#12868);
#4205=VERTEX_POINT('',#12871);
#5124=EDGE_CURVE('',#4187,#4188,#2590,.T.);
#5125=EDGE_CURVE('',#4188,#4189,#2591,.T.);
#5126=EDGE_CURVE('',#4189,#4190,#2592,.T.);
#5127=EDGE_CURVE('',#4187,#4190,#2593,.T.);
#5128=EDGE_CURVE('',#4188,#4191,#2594,.T.);
#5129=EDGE_CURVE('',#4191,#4192,#2595,.T.);
#5130=EDGE_CURVE('',#4192,#4189,#2596,.T.);
#5131=EDGE_CURVE('',#4191,#4193,#2597,.T.);
#5132=EDGE_CURVE('',#4193,#4194,#2598,.T.);
#5133=EDGE_CURVE('',#4194,#4192,#2599,.T.);
#5134=EDGE_CURVE('',#4193,#4195,#2600,.T.);
#5135=EDGE_CURVE('',#4195,#4196,#2601,.T.);
#5136=EDGE_CURVE('',#4196,#4194,#2602,.T.);
#5137=EDGE_CURVE('',#4195,#4197,#2603,.T.);
#5138=EDGE_CURVE('',#4197,#4198,#2604,.T.);
#5139=EDGE_CURVE('',#4198,#4196,#2605,.T.);
#5140=EDGE_CURVE('',#4197,#4187,#2606,.T.);
#5141=EDGE_CURVE('',#4190,#4198,#2607,.T.);
#5142=EDGE_CURVE('',#4199,#4199,#3578,.T.);
#5143=EDGE_CURVE('',#4200,#4200,#3579,.T.);
#5144=EDGE_CURVE('',#4201,#4201,#3580,.T.);
#5145=EDGE_CURVE('',#4201,#4200,#2608,.T.);
#5146=EDGE_CURVE('',#4202,#4202,#3581,.T.);
#5147=EDGE_CURVE('',#4202,#4201,#2609,.T.);
#5148=EDGE_CURVE('',#4203,#4203,#3582,.T.);
#5149=EDGE_CURVE('',#4203,#4202,#2610,.T.);
#5150=EDGE_CURVE('',#4204,#4204,#3583,.T.);
#5151=EDGE_CURVE('',#4205,#4205,#3584,.F.);
#5152=EDGE_CURVE('',#4205,#4204,#2611,.T.);
#5153=EDGE_CURVE('',#4199,#4205,#2612,.T.);
#6982=ORIENTED_EDGE('',*,*,#5124,.T.);
#6983=ORIENTED_EDGE('',*,*,#5125,.T.);
#6984=ORIENTED_EDGE('',*,*,#5126,.T.);
#6985=ORIENTED_EDGE('',*,*,#5127,.F.);
#6986=ORIENTED_EDGE('',*,*,#5128,.T.);
#6987=ORIENTED_EDGE('',*,*,#5129,.T.);
#6988=ORIENTED_EDGE('',*,*,#5130,.T.);
#6989=ORIENTED_EDGE('',*,*,#5125,.F.);
#6990=ORIENTED_EDGE('',*,*,#5131,.T.);
#6991=ORIENTED_EDGE('',*,*,#5132,.T.);
#6992=ORIENTED_EDGE('',*,*,#5133,.T.);
#6993=ORIENTED_EDGE('',*,*,#5129,.F.);
#6994=ORIENTED_EDGE('',*,*,#5134,.T.);
#6995=ORIENTED_EDGE('',*,*,#5135,.T.);
#6996=ORIENTED_EDGE('',*,*,#5136,.T.);
#6997=ORIENTED_EDGE('',*,*,#5132,.F.);
#6998=ORIENTED_EDGE('',*,*,#5137,.T.);
#6999=ORIENTED_EDGE('',*,*,#5138,.T.);
#7000=ORIENTED_EDGE('',*,*,#5139,.T.);
#7001=ORIENTED_EDGE('',*,*,#5135,.F.);
#7002=ORIENTED_EDGE('',*,*,#5140,.T.);
#7003=ORIENTED_EDGE('',*,*,#5127,.T.);
#7004=ORIENTED_EDGE('',*,*,#5141,.T.);
#7005=ORIENTED_EDGE('',*,*,#5138,.F.);
#7006=ORIENTED_EDGE('',*,*,#5140,.F.);
#7007=ORIENTED_EDGE('',*,*,#5137,.F.);
#7008=ORIENTED_EDGE('',*,*,#5134,.F.);
#7009=ORIENTED_EDGE('',*,*,#5131,.F.);
#7010=ORIENTED_EDGE('',*,*,#5128,.F.);
#7011=ORIENTED_EDGE('',*,*,#5124,.F.);
#7012=ORIENTED_EDGE('',*,*,#5141,.F.);
#7013=ORIENTED_EDGE('',*,*,#5126,.F.);
#7014=ORIENTED_EDGE('',*,*,#5130,.F.);
#7015=ORIENTED_EDGE('',*,*,#5133,.F.);
#7016=ORIENTED_EDGE('',*,*,#5136,.F.);
#7017=ORIENTED_EDGE('',*,*,#5139,.F.);
#7018=ORIENTED_EDGE('',*,*,#5142,.F.);
#7019=ORIENTED_EDGE('',*,*,#5143,.F.);
#7020=ORIENTED_EDGE('',*,*,#5144,.F.);
#7021=ORIENTED_EDGE('',*,*,#5145,.T.);
#7022=ORIENTED_EDGE('',*,*,#5143,.T.);
#7023=ORIENTED_EDGE('',*,*,#5145,.F.);
#7024=ORIENTED_EDGE('',*,*,#5146,.F.);
#7025=ORIENTED_EDGE('',*,*,#5147,.T.);
#7026=ORIENTED_EDGE('',*,*,#5144,.T.);
#7027=ORIENTED_EDGE('',*,*,#5147,.F.);
#7028=ORIENTED_EDGE('',*,*,#5148,.F.);
#7029=ORIENTED_EDGE('',*,*,#5149,.T.);
#7030=ORIENTED_EDGE('',*,*,#5146,.T.);
#7031=ORIENTED_EDGE('',*,*,#5149,.F.);
#7032=ORIENTED_EDGE('',*,*,#5148,.T.);
#7033=ORIENTED_EDGE('',*,*,#5150,.F.);
#7034=ORIENTED_EDGE('',*,*,#5151,.F.);
#7035=ORIENTED_EDGE('',*,*,#5152,.T.);
#7036=ORIENTED_EDGE('',*,*,#5150,.T.);
#7037=ORIENTED_EDGE('',*,*,#5152,.F.);
#7038=ORIENTED_EDGE('',*,*,#5142,.T.);
#7039=ORIENTED_EDGE('',*,*,#5153,.T.);
#7040=ORIENTED_EDGE('',*,*,#5151,.T.);
#7041=ORIENTED_EDGE('',*,*,#5153,.F.);
#7178=CYLINDRICAL_SURFACE('',#8588,0.425);
#7179=CYLINDRICAL_SURFACE('',#8596,0.24505);
#7564=ADVANCED_FACE('',(#1296),#892,.F.);
#7565=ADVANCED_FACE('',(#1297),#893,.F.);
#7566=ADVANCED_FACE('',(#1298),#894,.F.);
#7567=ADVANCED_FACE('',(#1299),#895,.F.);
#7568=ADVANCED_FACE('',(#1300),#896,.F.);
#7569=ADVANCED_FACE('',(#1301),#897,.F.);
#7570=ADVANCED_FACE('',(#1302),#898,.F.);
#7571=ADVANCED_FACE('',(#1303),#899,.F.);
#7572=ADVANCED_FACE('',(#1304),#900,.F.);
#7573=ADVANCED_FACE('',(#1305),#901,.T.);
#7574=ADVANCED_FACE('',(#1306),#339,.T.);
#7575=ADVANCED_FACE('',(#1307),#7178,.T.);
#7576=ADVANCED_FACE('',(#1308),#340,.T.);
#7577=ADVANCED_FACE('',(#1309,#588),#902,.T.);
#7578=ADVANCED_FACE('',(#1310),#341,.T.);
#7579=ADVANCED_FACE('',(#1311),#7179,.T.);
#7629=CLOSED_SHELL('',(#7564,#7565,#7566,#7567,#7568,#7569,#7570,#7571));
#7630=CLOSED_SHELL('',(#7572,#7573,#7574,#7575,#7576,#7577,#7578,#7579));
#8573=AXIS2_PLACEMENT_3D('',#12810,#10602,#10603);
#8574=AXIS2_PLACEMENT_3D('',#12811,#10604,#10605);
#8575=AXIS2_PLACEMENT_3D('',#12820,#10610,#10611);
#8576=AXIS2_PLACEMENT_3D('',#12826,#10615,#10616);
#8577=AXIS2_PLACEMENT_3D('',#12832,#10620,#10621);
#8578=AXIS2_PLACEMENT_3D('',#12838,#10625,#10626);
#8579=AXIS2_PLACEMENT_3D('',#12844,#10630,#10631);
#8580=AXIS2_PLACEMENT_3D('',#12847,#10634,#10635);
#8581=AXIS2_PLACEMENT_3D('',#12848,#10636,#10637);
#8582=AXIS2_PLACEMENT_3D('',#12849,#10638,#10639);
#8583=AXIS2_PLACEMENT_3D('',#12851,#10640,#10641);
#8584=AXIS2_PLACEMENT_3D('',#12852,#10642,#10643);
#8585=AXIS2_PLACEMENT_3D('',#12854,#10644,#10645);
#8586=AXIS2_PLACEMENT_3D('',#12855,#10646,#10647);
#8587=AXIS2_PLACEMENT_3D('',#12857,#10648,#10649);
#8588=AXIS2_PLACEMENT_3D('',#12859,#10651,#10652);
#8589=AXIS2_PLACEMENT_3D('',#12861,#10653,#10654);
#8590=AXIS2_PLACEMENT_3D('',#12863,#10656,#10657);
#8591=AXIS2_PLACEMENT_3D('',#12865,#10658,#10659);
#8592=AXIS2_PLACEMENT_3D('',#12867,#10661,#10662);
#8593=AXIS2_PLACEMENT_3D('',#12869,#10663,#10664);
#8594=AXIS2_PLACEMENT_3D('',#12870,#10665,#10666);
#8595=AXIS2_PLACEMENT_3D('',#12872,#10667,#10668);
#8596=AXIS2_PLACEMENT_3D('',#12874,#10670,#10671);
#10602=DIRECTION('axis',(0.,0.,1.));
#10603=DIRECTION('refdir',(1.,0.,0.));
#10604=DIRECTION('center_axis',(0.866025403784439,0.,-0.5));
#10605=DIRECTION('ref_axis',(0.5,0.,0.866025403784439));
#10606=DIRECTION('',(-0.5,0.,-0.866025403784439));
#10607=DIRECTION('',(0.,-1.,0.));
#10608=DIRECTION('',(0.5,0.,0.866025403784439));
#10609=DIRECTION('',(0.,-1.,0.));
#10610=DIRECTION('center_axis',(1.20185167898973E-16,0.,-1.));
#10611=DIRECTION('ref_axis',(1.,0.,1.20185167898973E-16));
#10612=DIRECTION('',(-1.,0.,-1.20185167898973E-16));
#10613=DIRECTION('',(0.,-1.,0.));
#10614=DIRECTION('',(1.,0.,1.20185167898973E-16));
#10615=DIRECTION('center_axis',(-0.866025403784439,0.,-0.5));
#10616=DIRECTION('ref_axis',(0.5,0.,-0.866025403784439));
#10617=DIRECTION('',(-0.5,0.,0.866025403784439));
#10618=DIRECTION('',(0.,-1.,0.));
#10619=DIRECTION('',(0.5,0.,-0.866025403784439));
#10620=DIRECTION('center_axis',(-0.866025403784439,0.,0.5));
#10621=DIRECTION('ref_axis',(-0.5,0.,-0.866025403784439));
#10622=DIRECTION('',(0.5,0.,0.866025403784439));
#10623=DIRECTION('',(0.,-1.,0.));
#10624=DIRECTION('',(-0.5,0.,-0.866025403784439));
#10625=DIRECTION('center_axis',(-2.40370335797945E-16,0.,1.));
#10626=DIRECTION('ref_axis',(-1.,0.,-2.40370335797945E-16));
#10627=DIRECTION('',(1.,0.,2.40370335797945E-16));
#10628=DIRECTION('',(0.,-1.,0.));
#10629=DIRECTION('',(-1.,0.,-2.40370335797945E-16));
#10630=DIRECTION('center_axis',(0.866025403784439,0.,0.5));
#10631=DIRECTION('ref_axis',(-0.5,0.,0.866025403784439));
#10632=DIRECTION('',(0.5,0.,-0.866025403784439));
#10633=DIRECTION('',(-0.5,0.,0.866025403784439));
#10634=DIRECTION('center_axis',(0.,1.,0.));
#10635=DIRECTION('ref_axis',(1.,0.,0.));
#10636=DIRECTION('center_axis',(0.,-1.,0.));
#10637=DIRECTION('ref_axis',(0.,0.,-1.));
#10638=DIRECTION('center_axis',(0.,1.,0.));
#10639=DIRECTION('ref_axis',(1.,0.,0.));
#10640=DIRECTION('center_axis',(0.,1.,0.));
#10641=DIRECTION('ref_axis',(1.,0.,0.));
#10642=DIRECTION('center_axis',(0.,1.,0.));
#10643=DIRECTION('ref_axis',(0.,0.,1.));
#10644=DIRECTION('center_axis',(0.,-1.,0.));
#10645=DIRECTION('ref_axis',(1.,0.,0.));
#10646=DIRECTION('center_axis',(0.,-1.,0.));
#10647=DIRECTION('ref_axis',(1.,0.,0.));
#10648=DIRECTION('center_axis',(0.,-1.,0.));
#10649=DIRECTION('ref_axis',(1.,0.,0.));
#10650=DIRECTION('',(0.707106781186548,0.707106781186547,8.65956056235493E-17));
#10651=DIRECTION('center_axis',(0.,-1.,0.));
#10652=DIRECTION('ref_axis',(1.,0.,0.));
#10653=DIRECTION('center_axis',(0.,-1.,0.));
#10654=DIRECTION('ref_axis',(1.,0.,0.));
#10655=DIRECTION('',(0.,1.,0.));
#10656=DIRECTION('center_axis',(0.,1.,0.));
#10657=DIRECTION('ref_axis',(1.,0.,0.));
#10658=DIRECTION('center_axis',(0.,-1.,0.));
#10659=DIRECTION('ref_axis',(1.,0.,0.));
#10660=DIRECTION('',(-0.707106781186547,0.707106781186548,-8.65956056235493E-17));
#10661=DIRECTION('center_axis',(0.,-1.,0.));
#10662=DIRECTION('ref_axis',(0.,0.,-1.));
#10663=DIRECTION('center_axis',(0.,-1.,0.));
#10664=DIRECTION('ref_axis',(1.,0.,0.));
#10665=DIRECTION('center_axis',(0.,1.,0.));
#10666=DIRECTION('ref_axis',(1.,0.,0.));
#10667=DIRECTION('center_axis',(0.,1.,0.));
#10668=DIRECTION('ref_axis',(1.,0.,0.));
#10669=DIRECTION('',(-0.447213595499958,0.894427190999916,-5.47678698264203E-17));
#10670=DIRECTION('center_axis',(0.,-1.,0.));
#10671=DIRECTION('ref_axis',(1.,0.,0.));
#10672=DIRECTION('',(0.,1.,0.));
#12810=CARTESIAN_POINT('',(0.,0.,0.));
#12811=CARTESIAN_POINT('Origin',(0.115470053837925,-0.5,-0.2));
#12812=CARTESIAN_POINT('',(0.23094010767585,-0.5,0.));
#12813=CARTESIAN_POINT('',(0.115470053837925,-0.5,-0.2));
#12814=CARTESIAN_POINT('',(0.23094010767585,-0.5,0.));
#12815=CARTESIAN_POINT('',(0.115470053837925,-0.8,-0.2));
#12816=CARTESIAN_POINT('',(0.115470053837925,-0.5,-0.2));
#12817=CARTESIAN_POINT('',(0.23094010767585,-0.8,0.));
#12818=CARTESIAN_POINT('',(0.23094010767585,-0.8,0.));
#12819=CARTESIAN_POINT('',(0.23094010767585,-0.5,0.));
#12820=CARTESIAN_POINT('Origin',(-0.115470053837925,-0.5,-0.2));
#12821=CARTESIAN_POINT('',(-0.115470053837925,-0.5,-0.2));
#12822=CARTESIAN_POINT('',(0.115470053837925,-0.5,-0.2));
#12823=CARTESIAN_POINT('',(-0.115470053837925,-0.8,-0.2));
#12824=CARTESIAN_POINT('',(-0.115470053837925,-0.5,-0.2));
#12825=CARTESIAN_POINT('',(0.115470053837925,-0.8,-0.2));
#12826=CARTESIAN_POINT('Origin',(-0.23094010767585,-0.5,-2.77555756156289E-17));
#12827=CARTESIAN_POINT('',(-0.23094010767585,-0.5,-2.82820063659975E-17));
#12828=CARTESIAN_POINT('',(-0.115470053837925,-0.5,-0.2));
#12829=CARTESIAN_POINT('',(-0.23094010767585,-0.8,-2.77555756156289E-17));
#12830=CARTESIAN_POINT('',(-0.23094010767585,-0.5,-2.82820063659975E-17));
#12831=CARTESIAN_POINT('',(-0.115470053837925,-0.8,-0.2));
#12832=CARTESIAN_POINT('Origin',(-0.115470053837925,-0.5,0.2));
#12833=CARTESIAN_POINT('',(-0.115470053837925,-0.5,0.2));
#12834=CARTESIAN_POINT('',(-0.23094010767585,-0.5,-2.82820063659975E-17));
#12835=CARTESIAN_POINT('',(-0.115470053837925,-0.8,0.2));
#12836=CARTESIAN_POINT('',(-0.115470053837925,-0.5,0.2));
#12837=CARTESIAN_POINT('',(-0.23094010767585,-0.8,-2.82820063659975E-17));
#12838=CARTESIAN_POINT('Origin',(0.115470053837925,-0.5,0.2));
#12839=CARTESIAN_POINT('',(0.115470053837925,-0.5,0.2));
#12840=CARTESIAN_POINT('',(-0.115470053837925,-0.5,0.2));
#12841=CARTESIAN_POINT('',(0.115470053837925,-0.8,0.2));
#12842=CARTESIAN_POINT('',(0.115470053837925,-0.5,0.2));
#12843=CARTESIAN_POINT('',(-0.115470053837925,-0.8,0.2));
#12844=CARTESIAN_POINT('Origin',(0.23094010767585,-0.5,0.));
#12845=CARTESIAN_POINT('',(0.115470053837925,-0.5,0.2));
#12846=CARTESIAN_POINT('',(0.115470053837925,-0.8,0.2));
#12847=CARTESIAN_POINT('Origin',(0.,-0.5,0.));
#12848=CARTESIAN_POINT('Origin',(0.,-0.8,0.));
#12849=CARTESIAN_POINT('Origin',(0.,-1.4,0.));
#12850=CARTESIAN_POINT('',(-0.24505,-1.4,3.00099698131059E-17));
#12851=CARTESIAN_POINT('Origin',(0.,-1.4,0.));
#12852=CARTESIAN_POINT('Origin',(0.375,0.5,0.));
#12853=CARTESIAN_POINT('',(-0.375,0.5,-4.59242549680257E-17));
#12854=CARTESIAN_POINT('Origin',(0.,0.5,0.));
#12855=CARTESIAN_POINT('Origin',(0.,0.475,0.));
#12856=CARTESIAN_POINT('',(-0.425,0.45,-5.20474889637625E-17));
#12857=CARTESIAN_POINT('Origin',(0.,0.45,0.));
#12858=CARTESIAN_POINT('',(-0.4,0.475,-4.89858719658941E-17));
#12859=CARTESIAN_POINT('Origin',(0.,0.24,0.));
#12860=CARTESIAN_POINT('',(-0.425,0.0299999999999998,-5.20474889637625E-17));
#12861=CARTESIAN_POINT('Origin',(0.,0.0299999999999998,0.));
#12862=CARTESIAN_POINT('',(-0.425,0.24,-5.20474889637625E-17));
#12863=CARTESIAN_POINT('Origin',(0.,0.0150000000000001,0.));
#12864=CARTESIAN_POINT('',(-0.395,4.85722573273506E-17,-4.83735485663204E-17));
#12865=CARTESIAN_POINT('Origin',(0.,0.,0.));
#12866=CARTESIAN_POINT('',(-0.41,0.0150000000000001,-5.02105187650415E-17));
#12867=CARTESIAN_POINT('Origin',(0.27,0.,0.));
#12868=CARTESIAN_POINT('',(-0.27,0.,-3.30654635769785E-17));
#12869=CARTESIAN_POINT('Origin',(0.,0.,0.));
#12870=CARTESIAN_POINT('Origin',(0.,-0.02,0.));
#12871=CARTESIAN_POINT('',(-0.24505,-0.0498999999999999,3.00099698131059E-17));
#12872=CARTESIAN_POINT('Origin',(0.,-0.0498999999999999,0.));
#12873=CARTESIAN_POINT('',(-0.26,-0.02,-3.18408167778312E-17));
#12874=CARTESIAN_POINT('Origin',(0.,-0.995,0.));
#12875=CARTESIAN_POINT('',(-0.24505,-0.995,-3.00099698131059E-17));
#13055=UNCERTAINTY_MEASURE_WITH_UNIT(LENGTH_MEASURE(0.001),#13095,
'DISTANCE_ACCURACY_VALUE',
'Maximum model space distance between geometric entities at asserted c
onnectivities');
#13057=UNCERTAINTY_MEASURE_WITH_UNIT(LENGTH_MEASURE(0.001),#13095,
'DISTANCE_ACCURACY_VALUE',
'Maximum model space distance between geometric entities at asserted c
onnectivities');
#13092=(
GEOMETRIC_REPRESENTATION_CONTEXT(3)
GLOBAL_UNCERTAINTY_ASSIGNED_CONTEXT((#13055))
GLOBAL_UNIT_ASSIGNED_CONTEXT((#13095,#13097,#13098))
REPRESENTATION_CONTEXT('','3D')
);
#13094=(
GEOMETRIC_REPRESENTATION_CONTEXT(3)
GLOBAL_UNCERTAINTY_ASSIGNED_CONTEXT((#13057))
GLOBAL_UNIT_ASSIGNED_CONTEXT((#13095,#13097,#13098))
REPRESENTATION_CONTEXT('','3D')
);
#13095=(
LENGTH_UNIT()
NAMED_UNIT(*)
SI_UNIT(.CENTI.,.METRE.)
);
#13097=(
NAMED_UNIT(*)
PLANE_ANGLE_UNIT()
SI_UNIT($,.RADIAN.)
);
#13098=(
NAMED_UNIT(*)
SI_UNIT($,.STERADIAN.)
SOLID_ANGLE_UNIT()
);
#13133=SHAPE_DEFINITION_REPRESENTATION(#13172,#13283);
#13172=PRODUCT_DEFINITION_SHAPE('',$,#13320);
#13283=SHAPE_REPRESENTATION('',(#8573),#13092);
#13285=PRODUCT_DEFINITION_CONTEXT('part definition',#13395,'design');
#13320=PRODUCT_DEFINITION('M5x14 Cap Screw','M5x14 Cap Screw',#13356,#13285);
#13356=PRODUCT_DEFINITION_FORMATION('',$,#13431);
#13395=APPLICATION_CONTEXT(
'Core Data for Automotive Mechanical Design Process');
#13396=PRODUCT_CONTEXT('part definition',#13395,'mechanical');
#13431=PRODUCT('M5x14 Cap Screw','M5x14 Cap Screw','M5x14 Cap Screw',(#13396));
#13496=COLOUR_RGB('Black',0.12,0.14,0.17);
#13497=FILL_AREA_STYLE_COLOUR('',#13496);
#13498=FILL_AREA_STYLE('',(#13497));
#13499=SURFACE_STYLE_FILL_AREA(#13498);
#13500=SURFACE_SIDE_STYLE('',(#13499));
#13501=SURFACE_STYLE_USAGE(.BOTH.,#13500);
#13502=PRESENTATION_STYLE_ASSIGNMENT((#13501));
ENDSEC;
END-ISO-10303-21;
